ISO-10303-21;
HEADER;
/* Generated by software containing ST-Developer
 * from STEP Tools, Inc. (www.steptools.com) 
 */

FILE_DESCRIPTION(
/* description */ ('Four-bar parallelogram arm'),
/* implementation_level */ '2;1');

FILE_NAME(
/* name */ 'Inner race sleeve (3).step',
/* time_stamp */ '2026-10-28T03:24:55-07:00',
/* author */ (''),
/* organization */ (''),
/* preprocessor_version */ 'ST-DEVELOPER v20.2',
/* originating_system */ 'Autodesk Translation Framework v15.17.0.0',
/* authorisation */ '');

FILE_SCHEMA (('AUTOMOTIVE_DESIGN { 1 0 10303 214 3 1 1 }'));
ENDSEC;

DATA;
#10=MECHANICAL_DESIGN_GEOMETRIC_PRESENTATION_REPRESENTATION('',(#675),#14512);
#567=SHAPE_REPRESENTATION_RELATIONSHIP('SRR','None',#14792,#617);
#617=ADVANCED_BREP_SHAPE_REPRESENTATION('',(#731),#14507);
#675=STYLED_ITEM('',(#15087),#731);
#731=MANIFOLD_SOLID_BREP('Body1',#7381);
#997=FACE_BOUND('',#2273,.T.);
#998=FACE_BOUND('',#2275,.T.);
#1182=PLANE('',#8863);
#1183=PLANE('',#8864);
#1588=FACE_OUTER_BOUND('',#2270,.T.);
#1589=FACE_OUTER_BOUND('',#2271,.T.);
#1590=FACE_OUTER_BOUND('',#2272,.T.);
#1591=FACE_OUTER_BOUND('',#2274,.T.);
#2270=EDGE_LOOP('',(#6602,#6603,#6604,#6605));
#2271=EDGE_LOOP('',(#6606,#6607,#6608,#6609));
#2272=EDGE_LOOP('',(#6610));
#2273=EDGE_LOOP('',(#6611));
#2274=EDGE_LOOP('',(#6612));
#2275=EDGE_LOOP('',(#6613));
#2674=LINE('',#14222,#3068);
#2675=LINE('',#14228,#3069);
#3068=VECTOR('',#11174,0.504999999999999);
#3069=VECTOR('',#11181,0.699999999999999);
#3521=CIRCLE('',#8858,0.504999999999999);
#3522=CIRCLE('',#8859,0.504999999999999);
#3523=CIRCLE('',#8861,0.699999999999999);
#3524=CIRCLE('',#8862,0.699999999999999);
#4089=VERTEX_POINT('',#14219);
#4090=VERTEX_POINT('',#14221);
#4091=VERTEX_POINT('',#14225);
#4092=VERTEX_POINT('',#14227);
#4932=EDGE_CURVE('',#4089,#4089,#3521,.T.);
#4933=EDGE_CURVE('',#4089,#4090,#2674,.T.);
#4934=EDGE_CURVE('',#4090,#4090,#3522,.T.);
#4935=EDGE_CURVE('',#4091,#4091,#3523,.T.);
#4936=EDGE_CURVE('',#4091,#4092,#2675,.T.);
#4937=EDGE_CURVE('',#4092,#4092,#3524,.T.);
#6602=ORIENTED_EDGE('',*,*,#4932,.F.);
#6603=ORIENTED_EDGE('',*,*,#4933,.T.);
#6604=ORIENTED_EDGE('',*,*,#4934,.T.);
#6605=ORIENTED_EDGE('',*,*,#4933,.F.);
#6606=ORIENTED_EDGE('',*,*,#4935,.F.);
#6607=ORIENTED_EDGE('',*,*,#4936,.T.);
#6608=ORIENTED_EDGE('',*,*,#4937,.T.);
#6609=ORIENTED_EDGE('',*,*,#4936,.F.);
#6610=ORIENTED_EDGE('',*,*,#4935,.T.);
#6611=ORIENTED_EDGE('',*,*,#4932,.T.);
#6612=ORIENTED_EDGE('',*,*,#4937,.F.);
#6613=ORIENTED_EDGE('',*,*,#4934,.F.);
#6896=CYLINDRICAL_SURFACE('',#8857,0.504999999999999);
#6897=CYLINDRICAL_SURFACE('',#8860,0.699999999999999);
#7293=ADVANCED_FACE('',(#1588),#6896,.F.);
#7294=ADVANCED_FACE('',(#1589),#6897,.T.);
#7295=ADVANCED_FACE('',(#1590,#997),#1182,.T.);
#7296=ADVANCED_FACE('',(#1591,#998),#1183,.F.);
#7381=CLOSED_SHELL('',(#7293,#7294,#7295,#7296));
#8856=AXIS2_PLACEMENT_3D('',#14217,#11168,#11169);
#8857=AXIS2_PLACEMENT_3D('',#14218,#11170,#11171);
#8858=AXIS2_PLACEMENT_3D('',#14220,#11172,#11173);
#8859=AXIS2_PLACEMENT_3D('',#14223,#11175,#11176);
#8860=AXIS2_PLACEMENT_3D('',#14224,#11177,#11178);
#8861=AXIS2_PLACEMENT_3D('',#14226,#11179,#11180);
#8862=AXIS2_PLACEMENT_3D('',#14229,#11182,#11183);
#8863=AXIS2_PLACEMENT_3D('',#14230,#11184,#11185);
#8864=AXIS2_PLACEMENT_3D('',#14231,#11186,#11187);
#11168=DIRECTION('axis',(0.,0.,1.));
#11169=DIRECTION('refdir',(1.,0.,0.));
#11170=DIRECTION('center_axis',(0.,1.,0.));
#11171=DIRECTION('ref_axis',(1.,0.,0.));
#11172=DIRECTION('center_axis',(0.,-1.,0.));
#11173=DIRECTION('ref_axis',(1.,0.,0.));
#11174=DIRECTION('',(0.,-1.,0.));
#11175=DIRECTION('center_axis',(0.,-1.,0.));
#11176=DIRECTION('ref_axis',(1.,0.,0.));
#11177=DIRECTION('center_axis',(0.,1.,0.));
#11178=DIRECTION('ref_axis',(1.,0.,0.));
#11179=DIRECTION('center_axis',(0.,1.,0.));
#11180=DIRECTION('ref_axis',(1.,0.,0.));
#11181=DIRECTION('',(0.,-1.,0.));
#11182=DIRECTION('center_axis',(0.,1.,0.));
#11183=DIRECTION('ref_axis',(1.,0.,0.));
#11184=DIRECTION('center_axis',(0.,1.,0.));
#11185=DIRECTION('ref_axis',(1.,0.,0.));
#11186=DIRECTION('center_axis',(0.,1.,0.));
#11187=DIRECTION('ref_axis',(1.,0.,0.));
#14217=CARTESIAN_POINT('',(0.,0.,0.));
#14218=CARTESIAN_POINT('Origin',(20.,-0.15,14.));
#14219=CARTESIAN_POINT('',(19.495,0.15,14.));
#14220=CARTESIAN_POINT('Origin',(20.,0.15,14.));
#14221=CARTESIAN_POINT('',(19.495,-0.15,14.));
#14222=CARTESIAN_POINT('',(19.495,-0.15,14.));
#14223=CARTESIAN_POINT('Origin',(20.,-0.15,14.));
#14224=CARTESIAN_POINT('Origin',(20.,-0.15,14.));
#14225=CARTESIAN_POINT('',(19.3,0.15,14.));
#14226=CARTESIAN_POINT('Origin',(20.,0.15,14.));
#14227=CARTESIAN_POINT('',(19.3,-0.15,14.));
#14228=CARTESIAN_POINT('',(19.3,-0.15,14.));
#14229=CARTESIAN_POINT('Origin',(20.,-0.15,14.));
#14230=CARTESIAN_POINT('Origin',(20.,0.15,14.));
#14231=CARTESIAN_POINT('Origin',(20.,-0.15,14.));
#14450=UNCERTAINTY_MEASURE_WITH_UNIT(LENGTH_MEASURE(0.001),#14513,
'DISTANCE_ACCURACY_VALUE',
'Maximum model space distance between geometric entities at asserted c
onnectivities');
#14455=UNCERTAINTY_MEASURE_WITH_UNIT(LENGTH_MEASURE(0.001),#14513,
'DISTANCE_ACCURACY_VALUE',
'Maximum model space distance between geometric entities at asserted c
onnectivities');
#14507=(
GEOMETRIC_REPRESENTATION_CONTEXT(3)
GLOBAL_UNCERTAINTY_ASSIGNED_CONTEXT((#14450))
GLOBAL_UNIT_ASSIGNED_CONTEXT((#14513,#14515,#14516))
REPRESENTATION_CONTEXT('','3D')
);
#14512=(
GEOMETRIC_REPRESENTATION_CONTEXT(3)
GLOBAL_UNCERTAINTY_ASSIGNED_CONTEXT((#14455))
GLOBAL_UNIT_ASSIGNED_CONTEXT((#14513,#14515,#14516))
REPRESENTATION_CONTEXT('','3D')
);
#14513=(
LENGTH_UNIT()
NAMED_UNIT(*)
SI_UNIT(.CENTI.,.METRE.)
);
#14515=(
NAMED_UNIT(*)
PLANE_ANGLE_UNIT()
SI_UNIT($,.RADIAN.)
);
#14516=(
NAMED_UNIT(*)
SI_UNIT($,.STERADIAN.)
SOLID_ANGLE_UNIT()
);
#14568=SHAPE_DEFINITION_REPRESENTATION(#14684,#14792);
#14684=PRODUCT_DEFINITION_SHAPE('',$,#14849);
#14792=SHAPE_REPRESENTATION('',(#8856),#14507);
#14797=PRODUCT_DEFINITION_CONTEXT('part definition',#14967,'design');
#14849=PRODUCT_DEFINITION('Inner race sleeve (3)','Inner race sleeve (3)',
#14905,#14797);
#14905=PRODUCT_DEFINITION_FORMATION('',$,#15020);
#14967=APPLICATION_CONTEXT(
'Core Data for Automotive Mechanical Design Process');
#14968=PRODUCT_CONTEXT('part definition',#14967,'mechanical');
#15020=PRODUCT('Inner race sleeve (3)','Inner race sleeve (3)',
'Inner race sleeve (3)',(#14968));
#15081=COLOUR_RGB('Grey',0.48,0.52,0.57);
#15082=FILL_AREA_STYLE_COLOUR('',#15081);
#15083=FILL_AREA_STYLE('',(#15082));
#15084=SURFACE_STYLE_FILL_AREA(#15083);
#15085=SURFACE_SIDE_STYLE('',(#15084));
#15086=SURFACE_STYLE_USAGE(.BOTH.,#15085);
#15087=PRESENTATION_STYLE_ASSIGNMENT((#15086));
ENDSEC;
END-ISO-10303-21;
